ISO-10303-21;
HEADER;
/* Generated by software containing ST-Developer
 * from STEP Tools, Inc. (www.steptools.com) 
 */

FILE_DESCRIPTION(
/* description */ ('Flywheel Crank-Slider'),
/* implementation_level */ '2;1');

FILE_NAME(
/* name */ 'Cap Screw - M5x20.step',
/* time_stamp */ '2026-10-28T03:23:13-07:00',
/* author */ (''),
/* organization */ (''),
/* preprocessor_version */ 'ST-DEVELOPER v20.2',
/* originating_system */ 'Autodesk Translation Framework v15.17.0.0',
/* authorisation */ '');

FILE_SCHEMA (('AUTOMOTIVE_DESIGN { 1 0 10303 214 3 1 1 }'));
ENDSEC;

DATA;
#10=MECHANICAL_DESIGN_GEOMETRIC_PRESENTATION_REPRESENTATION('',(#679),#17322);
#529=ORIENTED_CLOSED_SHELL('',*,#9058,.F.);
#534=CONICAL_SURFACE('',#9949,0.4,0.785398163397448);
#535=CONICAL_SURFACE('',#9953,0.41,0.785398163397448);
#536=CONICAL_SURFACE('',#9957,0.26,0.463647609000806);
#537=CONICAL_SURFACE('',#9961,0.225,0.785398163397448);
#559=BREP_WITH_VOIDS('Body1',#9057,(#529));
#575=SHAPE_REPRESENTATION_RELATIONSHIP('SRR','None',#17571,#627);
#627=ADVANCED_BREP_SHAPE_REPRESENTATION('',(#559),#17275);
#679=STYLED_ITEM('',(#17938),#559);
#861=FACE_BOUND('',#2068,.T.);
#1085=PLANE('',#9947);
#1086=PLANE('',#9955);
#1087=PLANE('',#9963);
#1088=PLANE('',#9964);
#1089=PLANE('',#9965);
#1090=PLANE('',#9966);
#1091=PLANE('',#9967);
#1092=PLANE('',#9968);
#1093=PLANE('',#9969);
#1094=PLANE('',#9970);
#1095=PLANE('',#9971);
#1452=FACE_OUTER_BOUND('',#2063,.T.);
#1453=FACE_OUTER_BOUND('',#2064,.T.);
#1454=FACE_OUTER_BOUND('',#2065,.T.);
#1455=FACE_OUTER_BOUND('',#2066,.T.);
#1456=FACE_OUTER_BOUND('',#2067,.T.);
#1457=FACE_OUTER_BOUND('',#2069,.T.);
#1458=FACE_OUTER_BOUND('',#2070,.T.);
#1459=FACE_OUTER_BOUND('',#2071,.T.);
#1460=FACE_OUTER_BOUND('',#2072,.T.);
#1461=FACE_OUTER_BOUND('',#2073,.T.);
#1462=FACE_OUTER_BOUND('',#2074,.T.);
#1463=FACE_OUTER_BOUND('',#2075,.T.);
#1464=FACE_OUTER_BOUND('',#2076,.T.);
#1465=FACE_OUTER_BOUND('',#2077,.T.);
#1466=FACE_OUTER_BOUND('',#2078,.T.);
#1467=FACE_OUTER_BOUND('',#2079,.T.);
#1468=FACE_OUTER_BOUND('',#2080,.T.);
#2063=EDGE_LOOP('',(#6654));
#2064=EDGE_LOOP('',(#6655,#6656,#6657,#6658));
#2065=EDGE_LOOP('',(#6659,#6660,#6661,#6662));
#2066=EDGE_LOOP('',(#6663,#6664,#6665,#6666));
#2067=EDGE_LOOP('',(#6667));
#2068=EDGE_LOOP('',(#6668));
#2069=EDGE_LOOP('',(#6669,#6670,#6671,#6672));
#2070=EDGE_LOOP('',(#6673,#6674,#6675,#6676));
#2071=EDGE_LOOP('',(#6677,#6678,#6679,#6680));
#2072=EDGE_LOOP('',(#6681));
#2073=EDGE_LOOP('',(#6682,#6683,#6684,#6685));
#2074=EDGE_LOOP('',(#6686,#6687,#6688,#6689));
#2075=EDGE_LOOP('',(#6690,#6691,#6692,#6693));
#2076=EDGE_LOOP('',(#6694,#6695,#6696,#6697));
#2077=EDGE_LOOP('',(#6698,#6699,#6700,#6701));
#2078=EDGE_LOOP('',(#6702,#6703,#6704,#6705));
#2079=EDGE_LOOP('',(#6706,#6707,#6708,#6709,#6710,#6711));
#2080=EDGE_LOOP('',(#6712,#6713,#6714,#6715,#6716,#6717));
#2766=LINE('',#14321,#3377);
#2767=LINE('',#14325,#3378);
#2768=LINE('',#14329,#3379);
#2769=LINE('',#14336,#3380);
#2770=LINE('',#14340,#3381);
#2771=LINE('',#14344,#3382);
#2772=LINE('',#14349,#3383);
#2773=LINE('',#14351,#3384);
#2774=LINE('',#14353,#3385);
#2775=LINE('',#14354,#3386);
#2776=LINE('',#14357,#3387);
#2777=LINE('',#14359,#3388);
#2778=LINE('',#14360,#3389);
#2779=LINE('',#14363,#3390);
#2780=LINE('',#14365,#3391);
#2781=LINE('',#14366,#3392);
#2782=LINE('',#14369,#3393);
#2783=LINE('',#14371,#3394);
#2784=LINE('',#14372,#3395);
#2785=LINE('',#14375,#3396);
#2786=LINE('',#14377,#3397);
#2787=LINE('',#14378,#3398);
#2788=LINE('',#14380,#3399);
#2789=LINE('',#14381,#3400);
#3377=VECTOR('',#11512,0.4);
#3378=VECTOR('',#11517,0.425);
#3379=VECTOR('',#11522,0.41);
#3380=VECTOR('',#11531,0.26);
#3381=VECTOR('',#11536,0.25);
#3382=VECTOR('',#11541,0.225);
#3383=VECTOR('',#11546,1.);
#3384=VECTOR('',#11547,1.);
#3385=VECTOR('',#11548,1.);
#3386=VECTOR('',#11549,1.);
#3387=VECTOR('',#11552,1.);
#3388=VECTOR('',#11553,1.);
#3389=VECTOR('',#11554,1.);
#3390=VECTOR('',#11557,1.);
#3391=VECTOR('',#11558,1.);
#3392=VECTOR('',#11559,1.);
#3393=VECTOR('',#11562,1.);
#3394=VECTOR('',#11563,1.);
#3395=VECTOR('',#11564,1.);
#3396=VECTOR('',#11567,1.);
#3397=VECTOR('',#11568,1.);
#3398=VECTOR('',#11569,1.);
#3399=VECTOR('',#11572,1.);
#3400=VECTOR('',#11573,1.);
#3954=CIRCLE('',#9948,0.375);
#3955=CIRCLE('',#9950,0.425);
#3956=CIRCLE('',#9952,0.425);
#3957=CIRCLE('',#9954,0.395);
#3958=CIRCLE('',#9956,0.27);
#3959=CIRCLE('',#9958,0.24505);
#3960=CIRCLE('',#9960,0.24505);
#3961=CIRCLE('',#9962,0.2);
#4449=VERTEX_POINT('',#14316);
#4450=VERTEX_POINT('',#14319);
#4451=VERTEX_POINT('',#14323);
#4452=VERTEX_POINT('',#14327);
#4453=VERTEX_POINT('',#14331);
#4454=VERTEX_POINT('',#14334);
#4455=VERTEX_POINT('',#14338);
#4456=VERTEX_POINT('',#14342);
#4457=VERTEX_POINT('',#14347);
#4458=VERTEX_POINT('',#14348);
#4459=VERTEX_POINT('',#14350);
#4460=VERTEX_POINT('',#14352);
#4461=VERTEX_POINT('',#14356);
#4462=VERTEX_POINT('',#14358);
#4463=VERTEX_POINT('',#14362);
#4464=VERTEX_POINT('',#14364);
#4465=VERTEX_POINT('',#14368);
#4466=VERTEX_POINT('',#14370);
#4467=VERTEX_POINT('',#14374);
#4468=VERTEX_POINT('',#14376);
#5284=EDGE_CURVE('',#4449,#4449,#3954,.T.);
#5285=EDGE_CURVE('',#4450,#4450,#3955,.T.);
#5286=EDGE_CURVE('',#4450,#4449,#2766,.T.);
#5287=EDGE_CURVE('',#4451,#4451,#3956,.T.);
#5288=EDGE_CURVE('',#4451,#4450,#2767,.T.);
#5289=EDGE_CURVE('',#4452,#4452,#3957,.T.);
#5290=EDGE_CURVE('',#4452,#4451,#2768,.T.);
#5291=EDGE_CURVE('',#4453,#4453,#3958,.T.);
#5292=EDGE_CURVE('',#4454,#4454,#3959,.F.);
#5293=EDGE_CURVE('',#4454,#4453,#2769,.T.);
#5294=EDGE_CURVE('',#4455,#4455,#3960,.F.);
#5295=EDGE_CURVE('',#4455,#4454,#2770,.T.);
#5296=EDGE_CURVE('',#4456,#4456,#3961,.T.);
#5297=EDGE_CURVE('',#4456,#4455,#2771,.T.);
#5298=EDGE_CURVE('',#4457,#4458,#2772,.T.);
#5299=EDGE_CURVE('',#4458,#4459,#2773,.T.);
#5300=EDGE_CURVE('',#4459,#4460,#2774,.T.);
#5301=EDGE_CURVE('',#4457,#4460,#2775,.T.);
#5302=EDGE_CURVE('',#4458,#4461,#2776,.T.);
#5303=EDGE_CURVE('',#4461,#4462,#2777,.T.);
#5304=EDGE_CURVE('',#4462,#4459,#2778,.T.);
#5305=EDGE_CURVE('',#4461,#4463,#2779,.T.);
#5306=EDGE_CURVE('',#4463,#4464,#2780,.T.);
#5307=EDGE_CURVE('',#4464,#4462,#2781,.T.);
#5308=EDGE_CURVE('',#4463,#4465,#2782,.T.);
#5309=EDGE_CURVE('',#4465,#4466,#2783,.T.);
#5310=EDGE_CURVE('',#4466,#4464,#2784,.T.);
#5311=EDGE_CURVE('',#4465,#4467,#2785,.T.);
#5312=EDGE_CURVE('',#4467,#4468,#2786,.T.);
#5313=EDGE_CURVE('',#4468,#4466,#2787,.T.);
#5314=EDGE_CURVE('',#4467,#4457,#2788,.T.);
#5315=EDGE_CURVE('',#4460,#4468,#2789,.T.);
#6654=ORIENTED_EDGE('',*,*,#5284,.F.);
#6655=ORIENTED_EDGE('',*,*,#5285,.F.);
#6656=ORIENTED_EDGE('',*,*,#5286,.T.);
#6657=ORIENTED_EDGE('',*,*,#5284,.T.);
#6658=ORIENTED_EDGE('',*,*,#5286,.F.);
#6659=ORIENTED_EDGE('',*,*,#5287,.F.);
#6660=ORIENTED_EDGE('',*,*,#5288,.T.);
#6661=ORIENTED_EDGE('',*,*,#5285,.T.);
#6662=ORIENTED_EDGE('',*,*,#5288,.F.);
#6663=ORIENTED_EDGE('',*,*,#5289,.F.);
#6664=ORIENTED_EDGE('',*,*,#5290,.T.);
#6665=ORIENTED_EDGE('',*,*,#5287,.T.);
#6666=ORIENTED_EDGE('',*,*,#5290,.F.);
#6667=ORIENTED_EDGE('',*,*,#5289,.T.);
#6668=ORIENTED_EDGE('',*,*,#5291,.F.);
#6669=ORIENTED_EDGE('',*,*,#5292,.F.);
#6670=ORIENTED_EDGE('',*,*,#5293,.T.);
#6671=ORIENTED_EDGE('',*,*,#5291,.T.);
#6672=ORIENTED_EDGE('',*,*,#5293,.F.);
#6673=ORIENTED_EDGE('',*,*,#5294,.F.);
#6674=ORIENTED_EDGE('',*,*,#5295,.T.);
#6675=ORIENTED_EDGE('',*,*,#5292,.T.);
#6676=ORIENTED_EDGE('',*,*,#5295,.F.);
#6677=ORIENTED_EDGE('',*,*,#5296,.F.);
#6678=ORIENTED_EDGE('',*,*,#5297,.T.);
#6679=ORIENTED_EDGE('',*,*,#5294,.T.);
#6680=ORIENTED_EDGE('',*,*,#5297,.F.);
#6681=ORIENTED_EDGE('',*,*,#5296,.T.);
#6682=ORIENTED_EDGE('',*,*,#5298,.T.);
#6683=ORIENTED_EDGE('',*,*,#5299,.T.);
#6684=ORIENTED_EDGE('',*,*,#5300,.T.);
#6685=ORIENTED_EDGE('',*,*,#5301,.F.);
#6686=ORIENTED_EDGE('',*,*,#5302,.T.);
#6687=ORIENTED_EDGE('',*,*,#5303,.T.);
#6688=ORIENTED_EDGE('',*,*,#5304,.T.);
#6689=ORIENTED_EDGE('',*,*,#5299,.F.);
#6690=ORIENTED_EDGE('',*,*,#5305,.T.);
#6691=ORIENTED_EDGE('',*,*,#5306,.T.);
#6692=ORIENTED_EDGE('',*,*,#5307,.T.);
#6693=ORIENTED_EDGE('',*,*,#5303,.F.);
#6694=ORIENTED_EDGE('',*,*,#5308,.T.);
#6695=ORIENTED_EDGE('',*,*,#5309,.T.);
#6696=ORIENTED_EDGE('',*,*,#5310,.T.);
#6697=ORIENTED_EDGE('',*,*,#5306,.F.);
#6698=ORIENTED_EDGE('',*,*,#5311,.T.);
#6699=ORIENTED_EDGE('',*,*,#5312,.T.);
#6700=ORIENTED_EDGE('',*,*,#5313,.T.);
#6701=ORIENTED_EDGE('',*,*,#5309,.F.);
#6702=ORIENTED_EDGE('',*,*,#5314,.T.);
#6703=ORIENTED_EDGE('',*,*,#5301,.T.);
#6704=ORIENTED_EDGE('',*,*,#5315,.T.);
#6705=ORIENTED_EDGE('',*,*,#5312,.F.);
#6706=ORIENTED_EDGE('',*,*,#5314,.F.);
#6707=ORIENTED_EDGE('',*,*,#5311,.F.);
#6708=ORIENTED_EDGE('',*,*,#5308,.F.);
#6709=ORIENTED_EDGE('',*,*,#5305,.F.);
#6710=ORIENTED_EDGE('',*,*,#5302,.F.);
#6711=ORIENTED_EDGE('',*,*,#5298,.F.);
#6712=ORIENTED_EDGE('',*,*,#5315,.F.);
#6713=ORIENTED_EDGE('',*,*,#5300,.F.);
#6714=ORIENTED_EDGE('',*,*,#5304,.F.);
#6715=ORIENTED_EDGE('',*,*,#5307,.F.);
#6716=ORIENTED_EDGE('',*,*,#5310,.F.);
#6717=ORIENTED_EDGE('',*,*,#5313,.F.);
#8388=CYLINDRICAL_SURFACE('',#9951,0.425);
#8389=CYLINDRICAL_SURFACE('',#9959,0.24505);
#8643=ADVANCED_FACE('',(#1452),#1085,.T.);
#8644=ADVANCED_FACE('',(#1453),#534,.T.);
#8645=ADVANCED_FACE('',(#1454),#8388,.T.);
#8646=ADVANCED_FACE('',(#1455),#535,.T.);
#8647=ADVANCED_FACE('',(#1456,#861),#1086,.T.);
#8648=ADVANCED_FACE('',(#1457),#536,.T.);
#8649=ADVANCED_FACE('',(#1458),#8389,.T.);
#8650=ADVANCED_FACE('',(#1459),#537,.T.);
#8651=ADVANCED_FACE('',(#1460),#1087,.T.);
#8652=ADVANCED_FACE('',(#1461),#1088,.F.);
#8653=ADVANCED_FACE('',(#1462),#1089,.F.);
#8654=ADVANCED_FACE('',(#1463),#1090,.F.);
#8655=ADVANCED_FACE('',(#1464),#1091,.F.);
#8656=ADVANCED_FACE('',(#1465),#1092,.F.);
#8657=ADVANCED_FACE('',(#1466),#1093,.F.);
#8658=ADVANCED_FACE('',(#1467),#1094,.F.);
#8659=ADVANCED_FACE('',(#1468),#1095,.F.);
#9057=CLOSED_SHELL('',(#8643,#8644,#8645,#8646,#8647,#8648,#8649,#8650,
#8651));
#9058=CLOSED_SHELL('',(#8652,#8653,#8654,#8655,#8656,#8657,#8658,#8659));
#9946=AXIS2_PLACEMENT_3D('',#14314,#11502,#11503);
#9947=AXIS2_PLACEMENT_3D('',#14315,#11504,#11505);
#9948=AXIS2_PLACEMENT_3D('',#14317,#11506,#11507);
#9949=AXIS2_PLACEMENT_3D('',#14318,#11508,#11509);
#9950=AXIS2_PLACEMENT_3D('',#14320,#11510,#11511);
#9951=AXIS2_PLACEMENT_3D('',#14322,#11513,#11514);
#9952=AXIS2_PLACEMENT_3D('',#14324,#11515,#11516);
#9953=AXIS2_PLACEMENT_3D('',#14326,#11518,#11519);
#9954=AXIS2_PLACEMENT_3D('',#14328,#11520,#11521);
#9955=AXIS2_PLACEMENT_3D('',#14330,#11523,#11524);
#9956=AXIS2_PLACEMENT_3D('',#14332,#11525,#11526);
#9957=AXIS2_PLACEMENT_3D('',#14333,#11527,#11528);
#9958=AXIS2_PLACEMENT_3D('',#14335,#11529,#11530);
#9959=AXIS2_PLACEMENT_3D('',#14337,#11532,#11533);
#9960=AXIS2_PLACEMENT_3D('',#14339,#11534,#11535);
#9961=AXIS2_PLACEMENT_3D('',#14341,#11537,#11538);
#9962=AXIS2_PLACEMENT_3D('',#14343,#11539,#11540);
#9963=AXIS2_PLACEMENT_3D('',#14345,#11542,#11543);
#9964=AXIS2_PLACEMENT_3D('',#14346,#11544,#11545);
#9965=AXIS2_PLACEMENT_3D('',#14355,#11550,#11551);
#9966=AXIS2_PLACEMENT_3D('',#14361,#11555,#11556);
#9967=AXIS2_PLACEMENT_3D('',#14367,#11560,#11561);
#9968=AXIS2_PLACEMENT_3D('',#14373,#11565,#11566);
#9969=AXIS2_PLACEMENT_3D('',#14379,#11570,#11571);
#9970=AXIS2_PLACEMENT_3D('',#14382,#11574,#11575);
#9971=AXIS2_PLACEMENT_3D('',#14383,#11576,#11577);
#11502=DIRECTION('axis',(0.,0.,1.));
#11503=DIRECTION('refdir',(1.,0.,0.));
#11504=DIRECTION('center_axis',(0.,1.,0.));
#11505=DIRECTION('ref_axis',(0.,0.,1.));
#11506=DIRECTION('center_axis',(0.,-1.,0.));
#11507=DIRECTION('ref_axis',(1.,0.,0.));
#11508=DIRECTION('center_axis',(0.,-1.,0.));
#11509=DIRECTION('ref_axis',(1.,0.,0.));
#11510=DIRECTION('center_axis',(0.,-1.,0.));
#11511=DIRECTION('ref_axis',(1.,0.,0.));
#11512=DIRECTION('',(0.707106781186548,0.707106781186547,8.65956056235493E-17));
#11513=DIRECTION('center_axis',(0.,-1.,0.));
#11514=DIRECTION('ref_axis',(1.,0.,0.));
#11515=DIRECTION('center_axis',(0.,-1.,0.));
#11516=DIRECTION('ref_axis',(1.,0.,0.));
#11517=DIRECTION('',(0.,1.,0.));
#11518=DIRECTION('center_axis',(0.,1.,0.));
#11519=DIRECTION('ref_axis',(1.,0.,0.));
#11520=DIRECTION('center_axis',(0.,-1.,0.));
#11521=DIRECTION('ref_axis',(1.,0.,0.));
#11522=DIRECTION('',(-0.707106781186547,0.707106781186548,-8.65956056235493E-17));
#11523=DIRECTION('center_axis',(0.,-1.,0.));
#11524=DIRECTION('ref_axis',(0.,0.,-1.));
#11525=DIRECTION('center_axis',(0.,-1.,0.));
#11526=DIRECTION('ref_axis',(1.,0.,0.));
#11527=DIRECTION('center_axis',(0.,1.,0.));
#11528=DIRECTION('ref_axis',(1.,0.,0.));
#11529=DIRECTION('center_axis',(0.,1.,0.));
#11530=DIRECTION('ref_axis',(1.,0.,0.));
#11531=DIRECTION('',(-0.447213595499958,0.894427190999916,-5.47678698264203E-17));
#11532=DIRECTION('center_axis',(0.,-1.,0.));
#11533=DIRECTION('ref_axis',(1.,0.,0.));
#11534=DIRECTION('center_axis',(0.,1.,0.));
#11535=DIRECTION('ref_axis',(1.,0.,0.));
#11536=DIRECTION('',(0.,1.,0.));
#11537=DIRECTION('center_axis',(0.,1.,0.));
#11538=DIRECTION('ref_axis',(1.,0.,0.));
#11539=DIRECTION('center_axis',(0.,-1.,0.));
#11540=DIRECTION('ref_axis',(1.,0.,0.));
#11541=DIRECTION('',(-0.707106781186547,0.707106781186548,-8.65956056235493E-17));
#11542=DIRECTION('center_axis',(0.,-1.,0.));
#11543=DIRECTION('ref_axis',(0.,0.,-1.));
#11544=DIRECTION('center_axis',(0.866025403784439,0.,-0.5));
#11545=DIRECTION('ref_axis',(0.5,0.,0.866025403784439));
#11546=DIRECTION('',(-0.5,0.,-0.866025403784439));
#11547=DIRECTION('',(0.,-1.,0.));
#11548=DIRECTION('',(0.5,0.,0.866025403784439));
#11549=DIRECTION('',(0.,-1.,0.));
#11550=DIRECTION('center_axis',(1.20185167898973E-16,0.,-1.));
#11551=DIRECTION('ref_axis',(1.,0.,1.20185167898973E-16));
#11552=DIRECTION('',(-1.,0.,-1.20185167898973E-16));
#11553=DIRECTION('',(0.,-1.,0.));
#11554=DIRECTION('',(1.,0.,1.20185167898973E-16));
#11555=DIRECTION('center_axis',(-0.866025403784439,0.,-0.5));
#11556=DIRECTION('ref_axis',(0.5,0.,-0.866025403784439));
#11557=DIRECTION('',(-0.5,0.,0.866025403784439));
#11558=DIRECTION('',(0.,-1.,0.));
#11559=DIRECTION('',(0.5,0.,-0.866025403784439));
#11560=DIRECTION('center_axis',(-0.866025403784439,0.,0.5));
#11561=DIRECTION('ref_axis',(-0.5,0.,-0.866025403784439));
#11562=DIRECTION('',(0.5,0.,0.866025403784439));
#11563=DIRECTION('',(0.,-1.,0.));
#11564=DIRECTION('',(-0.5,0.,-0.866025403784439));
#11565=DIRECTION('center_axis',(-2.40370335797945E-16,0.,1.));
#11566=DIRECTION('ref_axis',(-1.,0.,-2.40370335797945E-16));
#11567=DIRECTION('',(1.,0.,2.40370335797945E-16));
#11568=DIRECTION('',(0.,-1.,0.));
#11569=DIRECTION('',(-1.,0.,-2.40370335797945E-16));
#11570=DIRECTION('center_axis',(0.866025403784439,0.,0.5));
#11571=DIRECTION('ref_axis',(-0.5,0.,0.866025403784439));
#11572=DIRECTION('',(0.5,0.,-0.866025403784439));
#11573=DIRECTION('',(-0.5,0.,0.866025403784439));
#11574=DIRECTION('center_axis',(0.,1.,0.));
#11575=DIRECTION('ref_axis',(1.,0.,0.));
#11576=DIRECTION('center_axis',(0.,-1.,0.));
#11577=DIRECTION('ref_axis',(0.,0.,-1.));
#14314=CARTESIAN_POINT('',(0.,0.,0.));
#14315=CARTESIAN_POINT('Origin',(0.375,0.5,0.));
#14316=CARTESIAN_POINT('',(-0.375,0.5,-4.59242549680257E-17));
#14317=CARTESIAN_POINT('Origin',(0.,0.5,0.));
#14318=CARTESIAN_POINT('Origin',(0.,0.475,0.));
#14319=CARTESIAN_POINT('',(-0.425,0.45,-5.20474889637625E-17));
#14320=CARTESIAN_POINT('Origin',(0.,0.45,0.));
#14321=CARTESIAN_POINT('',(-0.4,0.475,-4.89858719658941E-17));
#14322=CARTESIAN_POINT('Origin',(0.,0.24,0.));
#14323=CARTESIAN_POINT('',(-0.425,0.0299999999999998,-5.20474889637625E-17));
#14324=CARTESIAN_POINT('Origin',(0.,0.0299999999999998,0.));
#14325=CARTESIAN_POINT('',(-0.425,0.24,-5.20474889637625E-17));
#14326=CARTESIAN_POINT('Origin',(0.,0.0150000000000001,0.));
#14327=CARTESIAN_POINT('',(-0.395,4.85722573273506E-17,-4.83735485663204E-17));
#14328=CARTESIAN_POINT('Origin',(0.,0.,0.));
#14329=CARTESIAN_POINT('',(-0.41,0.0150000000000001,-5.02105187650415E-17));
#14330=CARTESIAN_POINT('Origin',(0.27,0.,0.));
#14331=CARTESIAN_POINT('',(-0.27,0.,-3.30654635769785E-17));
#14332=CARTESIAN_POINT('Origin',(0.,0.,0.));
#14333=CARTESIAN_POINT('Origin',(0.,-0.02,0.));
#14334=CARTESIAN_POINT('',(-0.24505,-0.0498999999999999,3.00099698131059E-17));
#14335=CARTESIAN_POINT('Origin',(0.,-0.0498999999999999,0.));
#14336=CARTESIAN_POINT('',(-0.26,-0.02,-3.18408167778312E-17));
#14337=CARTESIAN_POINT('Origin',(0.,-0.995,0.));
#14338=CARTESIAN_POINT('',(-0.24505,-1.95495,3.00099698131059E-17));
#14339=CARTESIAN_POINT('Origin',(0.,-1.95495,0.));
#14340=CARTESIAN_POINT('',(-0.24505,-0.995,-3.00099698131059E-17));
#14341=CARTESIAN_POINT('Origin',(0.,-1.975,0.));
#14342=CARTESIAN_POINT('',(-0.2,-2.,-2.44929359829471E-17));
#14343=CARTESIAN_POINT('Origin',(0.,-2.,0.));
#14344=CARTESIAN_POINT('',(-0.225,-1.975,-2.75545529808154E-17));
#14345=CARTESIAN_POINT('Origin',(0.,-2.,0.));
#14346=CARTESIAN_POINT('Origin',(0.115470053837925,-0.5,-0.2));
#14347=CARTESIAN_POINT('',(0.23094010767585,-0.5,0.));
#14348=CARTESIAN_POINT('',(0.115470053837925,-0.5,-0.2));
#14349=CARTESIAN_POINT('',(0.23094010767585,-0.5,0.));
#14350=CARTESIAN_POINT('',(0.115470053837925,-0.8,-0.2));
#14351=CARTESIAN_POINT('',(0.115470053837925,-0.5,-0.2));
#14352=CARTESIAN_POINT('',(0.23094010767585,-0.8,0.));
#14353=CARTESIAN_POINT('',(0.23094010767585,-0.8,0.));
#14354=CARTESIAN_POINT('',(0.23094010767585,-0.5,0.));
#14355=CARTESIAN_POINT('Origin',(-0.115470053837925,-0.5,-0.2));
#14356=CARTESIAN_POINT('',(-0.115470053837925,-0.5,-0.2));
#14357=CARTESIAN_POINT('',(0.115470053837925,-0.5,-0.2));
#14358=CARTESIAN_POINT('',(-0.115470053837925,-0.8,-0.2));
#14359=CARTESIAN_POINT('',(-0.115470053837925,-0.5,-0.2));
#14360=CARTESIAN_POINT('',(0.115470053837925,-0.8,-0.2));
#14361=CARTESIAN_POINT('Origin',(-0.23094010767585,-0.5,-2.77555756156289E-17));
#14362=CARTESIAN_POINT('',(-0.23094010767585,-0.5,-2.82820063659975E-17));
#14363=CARTESIAN_POINT('',(-0.115470053837925,-0.5,-0.2));
#14364=CARTESIAN_POINT('',(-0.23094010767585,-0.8,-2.77555756156289E-17));
#14365=CARTESIAN_POINT('',(-0.23094010767585,-0.5,-2.82820063659975E-17));
#14366=CARTESIAN_POINT('',(-0.115470053837925,-0.8,-0.2));
#14367=CARTESIAN_POINT('Origin',(-0.115470053837925,-0.5,0.2));
#14368=CARTESIAN_POINT('',(-0.115470053837925,-0.5,0.2));
#14369=CARTESIAN_POINT('',(-0.23094010767585,-0.5,-2.82820063659975E-17));
#14370=CARTESIAN_POINT('',(-0.115470053837925,-0.8,0.2));
#14371=CARTESIAN_POINT('',(-0.115470053837925,-0.5,0.2));
#14372=CARTESIAN_POINT('',(-0.23094010767585,-0.8,-2.82820063659975E-17));
#14373=CARTESIAN_POINT('Origin',(0.115470053837925,-0.5,0.2));
#14374=CARTESIAN_POINT('',(0.115470053837925,-0.5,0.2));
#14375=CARTESIAN_POINT('',(-0.115470053837925,-0.5,0.2));
#14376=CARTESIAN_POINT('',(0.115470053837925,-0.8,0.2));
#14377=CARTESIAN_POINT('',(0.115470053837925,-0.5,0.2));
#14378=CARTESIAN_POINT('',(-0.115470053837925,-0.8,0.2));
#14379=CARTESIAN_POINT('Origin',(0.23094010767585,-0.5,0.));
#14380=CARTESIAN_POINT('',(0.115470053837925,-0.5,0.2));
#14381=CARTESIAN_POINT('',(0.115470053837925,-0.8,0.2));
#14382=CARTESIAN_POINT('Origin',(0.,-0.5,0.));
#14383=CARTESIAN_POINT('Origin',(0.,-0.8,0.));
#17214=UNCERTAINTY_MEASURE_WITH_UNIT(LENGTH_MEASURE(0.001),#17323,
'DISTANCE_ACCURACY_VALUE',
'Maximum model space distance between geometric entities at asserted c
onnectivities');
#17261=UNCERTAINTY_MEASURE_WITH_UNIT(LENGTH_MEASURE(0.001),#17323,
'DISTANCE_ACCURACY_VALUE',
'Maximum model space distance between geometric entities at asserted c
onnectivities');
#17275=(
GEOMETRIC_REPRESENTATION_CONTEXT(3)
GLOBAL_UNCERTAINTY_ASSIGNED_CONTEXT((#17214))
GLOBAL_UNIT_ASSIGNED_CONTEXT((#17323,#17325,#17326))
REPRESENTATION_CONTEXT('','3D')
);
#17322=(
GEOMETRIC_REPRESENTATION_CONTEXT(3)
GLOBAL_UNCERTAINTY_ASSIGNED_CONTEXT((#17261))
GLOBAL_UNIT_ASSIGNED_CONTEXT((#17323,#17325,#17326))
REPRESENTATION_CONTEXT('','3D')
);
#17323=(
LENGTH_UNIT()
NAMED_UNIT(*)
SI_UNIT(.CENTI.,.METRE.)
);
#17325=(
NAMED_UNIT(*)
PLANE_ANGLE_UNIT()
SI_UNIT($,.RADIAN.)
);
#17326=(
NAMED_UNIT(*)
SI_UNIT($,.STERADIAN.)
SOLID_ANGLE_UNIT()
);
#17340=SHAPE_DEFINITION_REPRESENTATION(#17400,#17571);
#17400=PRODUCT_DEFINITION_SHAPE('',$,#17632);
#17571=SHAPE_REPRESENTATION('',(#9946),#17275);
#17618=PRODUCT_DEFINITION_CONTEXT('part definition',#17800,'design');
#17632=PRODUCT_DEFINITION('Cap Screw - M5x20','Cap Screw - M5x20',#17692,
#17618);
#17692=PRODUCT_DEFINITION_FORMATION('',$,#17815);
#17800=APPLICATION_CONTEXT(
'Core Data for Automotive Mechanical Design Process');
#17801=PRODUCT_CONTEXT('part definition',#17800,'mechanical');
#17815=PRODUCT('Cap Screw - M5x20','Cap Screw - M5x20',
'Cap Screw - M5x20',(#17801));
#17932=COLOUR_RGB('Black',0.12,0.14,0.17);
#17933=FILL_AREA_STYLE_COLOUR('',#17932);
#17934=FILL_AREA_STYLE('',(#17933));
#17935=SURFACE_STYLE_FILL_AREA(#17934);
#17936=SURFACE_SIDE_STYLE('',(#17935));
#17937=SURFACE_STYLE_USAGE(.BOTH.,#17936);
#17938=PRESENTATION_STYLE_ASSIGNMENT((#17937));
ENDSEC;
END-ISO-10303-21;
